ISO-10303-21;
HEADER;
/* Generated by software containing ST-Developer
 * from STEP Tools, Inc. (www.steptools.com) 
 */

FILE_DESCRIPTION(
/* description */ (''),
/* implementation_level */ '2;1');

FILE_NAME(
/* name */ '17_Gauge_Plug_1-4_NPT.step',
/* time_stamp */ '2026-10-26T04:15:57-07:00',
/* author */ (''),
/* organization */ (''),
/* preprocessor_version */ 'ST-DEVELOPER v20.2',
/* originating_system */ 'Autodesk Translation Framework v15.15.0.0',
/* authorisation */ '');

FILE_SCHEMA (('AUTOMOTIVE_DESIGN { 1 0 10303 214 3 1 1 }'));
ENDSEC;

DATA;
#10=MECHANICAL_DESIGN_GEOMETRIC_PRESENTATION_REPRESENTATION('',(#470),#55737);
#410=CONICAL_SURFACE('',#29889,6.6,0.785398163397447);
#430=SHAPE_REPRESENTATION_RELATIONSHIP('SRR','None',#55839,#450);
#450=ADVANCED_BREP_SHAPE_REPRESENTATION('',(#490),#55735);
#470=STYLED_ITEM('',(#55984),#490);
#490=MANIFOLD_SOLID_BREP('Body1',#27239);
#754=FACE_BOUND('',#10055,.T.);
#755=FACE_BOUND('',#10070,.T.);
#1708=PLANE('',#29847);
#1709=PLANE('',#29848);
#1710=PLANE('',#29849);
#1711=PLANE('',#29850);
#1712=PLANE('',#29851);
#1713=PLANE('',#29852);
#1714=PLANE('',#29853);
#1715=PLANE('',#29854);
#1716=PLANE('',#29855);
#1717=PLANE('',#29856);
#1718=PLANE('',#29857);
#1719=PLANE('',#29858);
#1720=PLANE('',#29859);
#1721=PLANE('',#29860);
#1722=PLANE('',#29861);
#1723=PLANE('',#29862);
#1724=PLANE('',#29863);
#1725=PLANE('',#29864);
#1726=PLANE('',#29865);
#1727=PLANE('',#29866);
#1728=PLANE('',#29867);
#1729=PLANE('',#29868);
#1730=PLANE('',#29869);
#1731=PLANE('',#29870);
#1732=PLANE('',#29871);
#1733=PLANE('',#29872);
#1734=PLANE('',#29873);
#1735=PLANE('',#29874);
#1736=PLANE('',#29875);
#1737=PLANE('',#29876);
#1738=PLANE('',#29877);
#1739=PLANE('',#29878);
#1740=PLANE('',#29879);
#1741=PLANE('',#29880);
#1742=PLANE('',#29881);
#1743=PLANE('',#29882);
#1744=PLANE('',#29884);
#1745=PLANE('',#29885);
#1746=PLANE('',#29886);
#1747=PLANE('',#29887);
#4005=LINE('',#53438,#6376);
#4006=LINE('',#53440,#6377);
#4007=LINE('',#53441,#6378);
#4008=LINE('',#53445,#6379);
#4009=LINE('',#53446,#6380);
#4010=LINE('',#53447,#6381);
#4011=LINE('',#53451,#6382);
#4012=LINE('',#53453,#6383);
#4013=LINE('',#53454,#6384);
#4014=LINE('',#53458,#6385);
#4015=LINE('',#53459,#6386);
#4016=LINE('',#53460,#6387);
#4017=LINE('',#53462,#6388);
#4018=LINE('',#53463,#6389);
#4019=LINE('',#53467,#6390);
#4020=LINE('',#53469,#6391);
#4021=LINE('',#53470,#6392);
#4022=LINE('',#53474,#6393);
#4023=LINE('',#53475,#6394);
#4024=LINE('',#53476,#6395);
#4025=LINE('',#53480,#6396);
#4026=LINE('',#53482,#6397);
#4027=LINE('',#53483,#6398);
#4028=LINE('',#53487,#6399);
#4029=LINE('',#53488,#6400);
#4030=LINE('',#53489,#6401);
#4031=LINE('',#53491,#6402);
#4032=LINE('',#53492,#6403);
#4033=LINE('',#53496,#6404);
#4034=LINE('',#53498,#6405);
#4035=LINE('',#53499,#6406);
#4036=LINE('',#53503,#6407);
#4037=LINE('',#53504,#6408);
#4038=LINE('',#53505,#6409);
#4039=LINE('',#53509,#6410);
#4040=LINE('',#53511,#6411);
#4041=LINE('',#53512,#6412);
#4042=LINE('',#53516,#6413);
#4043=LINE('',#53517,#6414);
#4044=LINE('',#53518,#6415);
#4045=LINE('',#53520,#6416);
#4046=LINE('',#53521,#6417);
#4047=LINE('',#53523,#6418);
#4048=LINE('',#53524,#6419);
#4049=LINE('',#53526,#6420);
#4050=LINE('',#53527,#6421);
#4051=LINE('',#53529,#6422);
#4052=LINE('',#53530,#6423);
#4053=LINE('',#53532,#6424);
#4054=LINE('',#53534,#6425);
#4055=LINE('',#53536,#6426);
#4056=LINE('',#53540,#6427);
#4057=LINE('',#53542,#6428);
#4058=LINE('',#53544,#6429);
#4059=LINE('',#53546,#6430);
#4060=LINE('',#53548,#6431);
#4061=LINE('',#53549,#6432);
#4062=LINE('',#53552,#6433);
#4063=LINE('',#53554,#6434);
#4064=LINE('',#53555,#6435);
#4065=LINE('',#53558,#6436);
#4066=LINE('',#53559,#6437);
#4067=LINE('',#53562,#6438);
#4068=LINE('',#53564,#6439);
#4069=LINE('',#53565,#6440);
#4070=LINE('',#53568,#6441);
#4071=LINE('',#53569,#6442);
#4072=LINE('',#53571,#6443);
#4073=LINE('',#53573,#6444);
#4074=LINE('',#53576,#6445);
#4075=LINE('',#53578,#6446);
#4076=LINE('',#53579,#6447);
#4077=LINE('',#53582,#6448);
#4078=LINE('',#53583,#6449);
#4079=LINE('',#53586,#6450);
#4080=LINE('',#53587,#6451);
#4081=LINE('',#53590,#6452);
#4082=LINE('',#53591,#6453);
#4083=LINE('',#53594,#6454);
#4084=LINE('',#53595,#6455);
#4085=LINE('',#53597,#6456);
#4086=LINE('',#53600,#6457);
#4087=LINE('',#53601,#6458);
#4088=LINE('',#53602,#6459);
#4089=LINE('',#53614,#6460);
#4090=LINE('',#53616,#6461);
#6376=VECTOR('',#36995,10.);
#6377=VECTOR('',#36996,10.);
#6378=VECTOR('',#36997,10.);
#6379=VECTOR('',#37000,10.);
#6380=VECTOR('',#37001,10.);
#6381=VECTOR('',#37002,10.);
#6382=VECTOR('',#37005,10.);
#6383=VECTOR('',#37006,10.);
#6384=VECTOR('',#37007,10.);
#6385=VECTOR('',#37010,10.);
#6386=VECTOR('',#37011,10.);
#6387=VECTOR('',#37012,10.);
#6388=VECTOR('',#37015,10.);
#6389=VECTOR('',#37016,10.);
#6390=VECTOR('',#37019,10.);
#6391=VECTOR('',#37020,10.);
#6392=VECTOR('',#37021,10.);
#6393=VECTOR('',#37024,10.);
#6394=VECTOR('',#37025,10.);
#6395=VECTOR('',#37026,10.);
#6396=VECTOR('',#37029,10.);
#6397=VECTOR('',#37030,10.);
#6398=VECTOR('',#37031,10.);
#6399=VECTOR('',#37034,10.);
#6400=VECTOR('',#37035,10.);
#6401=VECTOR('',#37036,10.);
#6402=VECTOR('',#37039,10.);
#6403=VECTOR('',#37040,10.);
#6404=VECTOR('',#37043,10.);
#6405=VECTOR('',#37044,10.);
#6406=VECTOR('',#37045,10.);
#6407=VECTOR('',#37048,10.);
#6408=VECTOR('',#37049,10.);
#6409=VECTOR('',#37050,10.);
#6410=VECTOR('',#37053,10.);
#6411=VECTOR('',#37054,10.);
#6412=VECTOR('',#37055,10.);
#6413=VECTOR('',#37058,10.);
#6414=VECTOR('',#37059,10.);
#6415=VECTOR('',#37060,10.);
#6416=VECTOR('',#37063,10.);
#6417=VECTOR('',#37064,10.);
#6418=VECTOR('',#37067,10.);
#6419=VECTOR('',#37068,10.);
#6420=VECTOR('',#37071,10.);
#6421=VECTOR('',#37072,10.);
#6422=VECTOR('',#37075,10.);
#6423=VECTOR('',#37076,10.);
#6424=VECTOR('',#37079,10.);
#6425=VECTOR('',#37082,10.);
#6426=VECTOR('',#37085,10.);
#6427=VECTOR('',#37088,10.);
#6428=VECTOR('',#37089,10.);
#6429=VECTOR('',#37090,10.);
#6430=VECTOR('',#37091,10.);
#6431=VECTOR('',#37092,10.);
#6432=VECTOR('',#37093,10.);
#6433=VECTOR('',#37096,10.);
#6434=VECTOR('',#37097,10.);
#6435=VECTOR('',#37098,10.);
#6436=VECTOR('',#37101,10.);
#6437=VECTOR('',#37102,10.);
#6438=VECTOR('',#37105,10.);
#6439=VECTOR('',#37106,10.);
#6440=VECTOR('',#37107,10.);
#6441=VECTOR('',#37110,10.);
#6442=VECTOR('',#37111,10.);
#6443=VECTOR('',#37114,10.);
#6444=VECTOR('',#37117,10.);
#6445=VECTOR('',#37120,10.);
#6446=VECTOR('',#37121,10.);
#6447=VECTOR('',#37122,10.);
#6448=VECTOR('',#37125,10.);
#6449=VECTOR('',#37126,10.);
#6450=VECTOR('',#37129,10.);
#6451=VECTOR('',#37130,10.);
#6452=VECTOR('',#37133,10.);
#6453=VECTOR('',#37134,10.);
#6454=VECTOR('',#37137,10.);
#6455=VECTOR('',#37138,10.);
#6456=VECTOR('',#37141,10.);
#6457=VECTOR('',#37146,10.);
#6458=VECTOR('',#37147,10.);
#6459=VECTOR('',#37148,10.);
#6460=VECTOR('',#37165,6.6);
#6461=VECTOR('',#37168,6.85);
#6799=CYLINDRICAL_SURFACE('',#29891,6.85);
#8314=FACE_OUTER_BOUND('',#10033,.T.);
#8315=FACE_OUTER_BOUND('',#10034,.T.);
#8316=FACE_OUTER_BOUND('',#10035,.T.);
#8317=FACE_OUTER_BOUND('',#10036,.T.);
#8318=FACE_OUTER_BOUND('',#10037,.T.);
#8319=FACE_OUTER_BOUND('',#10038,.T.);
#8320=FACE_OUTER_BOUND('',#10039,.T.);
#8321=FACE_OUTER_BOUND('',#10040,.T.);
#8322=FACE_OUTER_BOUND('',#10041,.T.);
#8323=FACE_OUTER_BOUND('',#10042,.T.);
#8324=FACE_OUTER_BOUND('',#10043,.T.);
#8325=FACE_OUTER_BOUND('',#10044,.T.);
#8326=FACE_OUTER_BOUND('',#10045,.T.);
#8327=FACE_OUTER_BOUND('',#10046,.T.);
#8328=FACE_OUTER_BOUND('',#10047,.T.);
#8329=FACE_OUTER_BOUND('',#10048,.T.);
#8330=FACE_OUTER_BOUND('',#10049,.T.);
#8331=FACE_OUTER_BOUND('',#10050,.T.);
#8332=FACE_OUTER_BOUND('',#10051,.T.);
#8333=FACE_OUTER_BOUND('',#10052,.T.);
#8334=FACE_OUTER_BOUND('',#10053,.T.);
#8335=FACE_OUTER_BOUND('',#10054,.T.);
#8336=FACE_OUTER_BOUND('',#10056,.T.);
#8337=FACE_OUTER_BOUND('',#10057,.T.);
#8338=FACE_OUTER_BOUND('',#10058,.T.);
#8339=FACE_OUTER_BOUND('',#10059,.T.);
#8340=FACE_OUTER_BOUND('',#10060,.T.);
#8341=FACE_OUTER_BOUND('',#10061,.T.);
#8342=FACE_OUTER_BOUND('',#10062,.T.);
#8343=FACE_OUTER_BOUND('',#10063,.T.);
#8344=FACE_OUTER_BOUND('',#10064,.T.);
#8345=FACE_OUTER_BOUND('',#10065,.T.);
#8346=FACE_OUTER_BOUND('',#10066,.T.);
#8347=FACE_OUTER_BOUND('',#10067,.T.);
#8348=FACE_OUTER_BOUND('',#10068,.T.);
#8349=FACE_OUTER_BOUND('',#10069,.T.);
#8350=FACE_OUTER_BOUND('',#10071,.T.);
#8351=FACE_OUTER_BOUND('',#10072,.T.);
#8352=FACE_OUTER_BOUND('',#10073,.T.);
#8353=FACE_OUTER_BOUND('',#10074,.T.);
#8354=FACE_OUTER_BOUND('',#10075,.T.);
#8355=FACE_OUTER_BOUND('',#10076,.T.);
#10033=EDGE_LOOP('',(#25196,#25197,#25198));
#10034=EDGE_LOOP('',(#25199,#25200,#25201,#25202));
#10035=EDGE_LOOP('',(#25203,#25204,#25205));
#10036=EDGE_LOOP('',(#25206,#25207,#25208,#25209));
#10037=EDGE_LOOP('',(#25210,#25211,#25212,#25213));
#10038=EDGE_LOOP('',(#25214,#25215,#25216));
#10039=EDGE_LOOP('',(#25217,#25218,#25219,#25220));
#10040=EDGE_LOOP('',(#25221,#25222,#25223));
#10041=EDGE_LOOP('',(#25224,#25225,#25226,#25227));
#10042=EDGE_LOOP('',(#25228,#25229,#25230,#25231));
#10043=EDGE_LOOP('',(#25232,#25233,#25234));
#10044=EDGE_LOOP('',(#25235,#25236,#25237,#25238));
#10045=EDGE_LOOP('',(#25239,#25240,#25241));
#10046=EDGE_LOOP('',(#25242,#25243,#25244,#25245));
#10047=EDGE_LOOP('',(#25246,#25247,#25248,#25249));
#10048=EDGE_LOOP('',(#25250,#25251,#25252,#25253));
#10049=EDGE_LOOP('',(#25254,#25255,#25256,#25257));
#10050=EDGE_LOOP('',(#25258,#25259,#25260,#25261));
#10051=EDGE_LOOP('',(#25262,#25263,#25264,#25265));
#10052=EDGE_LOOP('',(#25266,#25267,#25268,#25269));
#10053=EDGE_LOOP('',(#25270,#25271,#25272,#25273));
#10054=EDGE_LOOP('',(#25274,#25275,#25276,#25277,#25278,#25279));
#10055=EDGE_LOOP('',(#25280,#25281,#25282,#25283,#25284,#25285));
#10056=EDGE_LOOP('',(#25286,#25287,#25288,#25289));
#10057=EDGE_LOOP('',(#25290,#25291,#25292,#25293));
#10058=EDGE_LOOP('',(#25294,#25295,#25296,#25297));
#10059=EDGE_LOOP('',(#25298,#25299,#25300,#25301));
#10060=EDGE_LOOP('',(#25302,#25303,#25304,#25305));
#10061=EDGE_LOOP('',(#25306,#25307,#25308,#25309));
#10062=EDGE_LOOP('',(#25310,#25311,#25312,#25313));
#10063=EDGE_LOOP('',(#25314,#25315,#25316,#25317));
#10064=EDGE_LOOP('',(#25318,#25319,#25320,#25321));
#10065=EDGE_LOOP('',(#25322,#25323,#25324,#25325));
#10066=EDGE_LOOP('',(#25326,#25327,#25328,#25329));
#10067=EDGE_LOOP('',(#25330,#25331,#25332,#25333));
#10068=EDGE_LOOP('',(#25334,#25335,#25336,#25337,#25338,#25339));
#10069=EDGE_LOOP('',(#25340,#25341,#25342,#25343,#25344,#25345,#25346,#25347,
#25348,#25349,#25350,#25351));
#10070=EDGE_LOOP('',(#25352));
#10071=EDGE_LOOP('',(#25353,#25354,#25355,#25356));
#10072=EDGE_LOOP('',(#25357,#25358,#25359,#25360));
#10073=EDGE_LOOP('',(#25361,#25362,#25363,#25364));
#10074=EDGE_LOOP('',(#25365));
#10075=EDGE_LOOP('',(#25366,#25367,#25368,#25369));
#10076=EDGE_LOOP('',(#25370,#25371,#25372,#25373));
#10966=CIRCLE('',#29883,6.85);
#10967=CIRCLE('',#29888,6.35);
#10968=CIRCLE('',#29890,6.85);
#13781=VERTEX_POINT('',#53436);
#13782=VERTEX_POINT('',#53437);
#13783=VERTEX_POINT('',#53439);
#13784=VERTEX_POINT('',#53443);
#13785=VERTEX_POINT('',#53444);
#13786=VERTEX_POINT('',#53449);
#13787=VERTEX_POINT('',#53450);
#13788=VERTEX_POINT('',#53452);
#13789=VERTEX_POINT('',#53456);
#13790=VERTEX_POINT('',#53457);
#13791=VERTEX_POINT('',#53465);
#13792=VERTEX_POINT('',#53466);
#13793=VERTEX_POINT('',#53468);
#13794=VERTEX_POINT('',#53472);
#13795=VERTEX_POINT('',#53473);
#13796=VERTEX_POINT('',#53478);
#13797=VERTEX_POINT('',#53479);
#13798=VERTEX_POINT('',#53481);
#13799=VERTEX_POINT('',#53485);
#13800=VERTEX_POINT('',#53486);
#13801=VERTEX_POINT('',#53494);
#13802=VERTEX_POINT('',#53495);
#13803=VERTEX_POINT('',#53497);
#13804=VERTEX_POINT('',#53501);
#13805=VERTEX_POINT('',#53502);
#13806=VERTEX_POINT('',#53507);
#13807=VERTEX_POINT('',#53508);
#13808=VERTEX_POINT('',#53510);
#13809=VERTEX_POINT('',#53514);
#13810=VERTEX_POINT('',#53515);
#13811=VERTEX_POINT('',#53538);
#13812=VERTEX_POINT('',#53539);
#13813=VERTEX_POINT('',#53541);
#13814=VERTEX_POINT('',#53543);
#13815=VERTEX_POINT('',#53545);
#13816=VERTEX_POINT('',#53547);
#13817=VERTEX_POINT('',#53551);
#13818=VERTEX_POINT('',#53553);
#13819=VERTEX_POINT('',#53557);
#13820=VERTEX_POINT('',#53561);
#13821=VERTEX_POINT('',#53563);
#13822=VERTEX_POINT('',#53567);
#13823=VERTEX_POINT('',#53575);
#13824=VERTEX_POINT('',#53577);
#13825=VERTEX_POINT('',#53581);
#13826=VERTEX_POINT('',#53585);
#13827=VERTEX_POINT('',#53589);
#13828=VERTEX_POINT('',#53593);
#13829=VERTEX_POINT('',#53603);
#13830=VERTEX_POINT('',#53609);
#13831=VERTEX_POINT('',#53612);
#17602=EDGE_CURVE('',#13781,#13782,#4005,.T.);
#17603=EDGE_CURVE('',#13783,#13781,#4006,.T.);
#17604=EDGE_CURVE('',#13782,#13783,#4007,.T.);
#17605=EDGE_CURVE('',#13784,#13785,#4008,.T.);
#17606=EDGE_CURVE('',#13785,#13783,#4009,.T.);
#17607=EDGE_CURVE('',#13781,#13784,#4010,.T.);
#17608=EDGE_CURVE('',#13786,#13787,#4011,.T.);
#17609=EDGE_CURVE('',#13788,#13786,#4012,.T.);
#17610=EDGE_CURVE('',#13787,#13788,#4013,.T.);
#17611=EDGE_CURVE('',#13789,#13790,#4014,.T.);
#17612=EDGE_CURVE('',#13790,#13788,#4015,.T.);
#17613=EDGE_CURVE('',#13786,#13789,#4016,.T.);
#17614=EDGE_CURVE('',#13782,#13787,#4017,.T.);
#17615=EDGE_CURVE('',#13788,#13781,#4018,.T.);
#17616=EDGE_CURVE('',#13791,#13792,#4019,.T.);
#17617=EDGE_CURVE('',#13793,#13791,#4020,.T.);
#17618=EDGE_CURVE('',#13792,#13793,#4021,.T.);
#17619=EDGE_CURVE('',#13794,#13795,#4022,.T.);
#17620=EDGE_CURVE('',#13795,#13793,#4023,.T.);
#17621=EDGE_CURVE('',#13791,#13794,#4024,.T.);
#17622=EDGE_CURVE('',#13796,#13797,#4025,.T.);
#17623=EDGE_CURVE('',#13798,#13796,#4026,.T.);
#17624=EDGE_CURVE('',#13797,#13798,#4027,.T.);
#17625=EDGE_CURVE('',#13799,#13800,#4028,.T.);
#17626=EDGE_CURVE('',#13800,#13798,#4029,.T.);
#17627=EDGE_CURVE('',#13796,#13799,#4030,.T.);
#17628=EDGE_CURVE('',#13787,#13797,#4031,.T.);
#17629=EDGE_CURVE('',#13798,#13786,#4032,.T.);
#17630=EDGE_CURVE('',#13801,#13802,#4033,.T.);
#17631=EDGE_CURVE('',#13803,#13801,#4034,.T.);
#17632=EDGE_CURVE('',#13802,#13803,#4035,.T.);
#17633=EDGE_CURVE('',#13804,#13805,#4036,.T.);
#17634=EDGE_CURVE('',#13805,#13803,#4037,.T.);
#17635=EDGE_CURVE('',#13801,#13804,#4038,.T.);
#17636=EDGE_CURVE('',#13806,#13807,#4039,.T.);
#17637=EDGE_CURVE('',#13808,#13806,#4040,.T.);
#17638=EDGE_CURVE('',#13807,#13808,#4041,.T.);
#17639=EDGE_CURVE('',#13809,#13810,#4042,.T.);
#17640=EDGE_CURVE('',#13810,#13808,#4043,.T.);
#17641=EDGE_CURVE('',#13806,#13809,#4044,.T.);
#17642=EDGE_CURVE('',#13797,#13807,#4045,.T.);
#17643=EDGE_CURVE('',#13808,#13796,#4046,.T.);
#17644=EDGE_CURVE('',#13807,#13802,#4047,.T.);
#17645=EDGE_CURVE('',#13803,#13806,#4048,.T.);
#17646=EDGE_CURVE('',#13802,#13792,#4049,.T.);
#17647=EDGE_CURVE('',#13793,#13801,#4050,.T.);
#17648=EDGE_CURVE('',#13792,#13782,#4051,.T.);
#17649=EDGE_CURVE('',#13783,#13791,#4052,.T.);
#17650=EDGE_CURVE('',#13790,#13784,#4053,.T.);
#17651=EDGE_CURVE('',#13800,#13789,#4054,.T.);
#17652=EDGE_CURVE('',#13810,#13799,#4055,.T.);
#17653=EDGE_CURVE('',#13811,#13812,#4056,.T.);
#17654=EDGE_CURVE('',#13813,#13811,#4057,.T.);
#17655=EDGE_CURVE('',#13814,#13813,#4058,.T.);
#17656=EDGE_CURVE('',#13815,#13814,#4059,.T.);
#17657=EDGE_CURVE('',#13816,#13815,#4060,.T.);
#17658=EDGE_CURVE('',#13812,#13816,#4061,.T.);
#17659=EDGE_CURVE('',#13814,#13817,#4062,.T.);
#17660=EDGE_CURVE('',#13817,#13818,#4063,.T.);
#17661=EDGE_CURVE('',#13815,#13818,#4064,.T.);
#17662=EDGE_CURVE('',#13813,#13819,#4065,.T.);
#17663=EDGE_CURVE('',#13819,#13817,#4066,.T.);
#17664=EDGE_CURVE('',#13812,#13820,#4067,.T.);
#17665=EDGE_CURVE('',#13820,#13821,#4068,.T.);
#17666=EDGE_CURVE('',#13821,#13811,#4069,.T.);
#17667=EDGE_CURVE('',#13822,#13820,#4070,.T.);
#17668=EDGE_CURVE('',#13816,#13822,#4071,.T.);
#17669=EDGE_CURVE('',#13821,#13819,#4072,.T.);
#17670=EDGE_CURVE('',#13818,#13822,#4073,.T.);
#17671=EDGE_CURVE('',#13819,#13823,#4074,.T.);
#17672=EDGE_CURVE('',#13823,#13824,#4075,.T.);
#17673=EDGE_CURVE('',#13817,#13824,#4076,.T.);
#17674=EDGE_CURVE('',#13821,#13825,#4077,.T.);
#17675=EDGE_CURVE('',#13825,#13823,#4078,.T.);
#17676=EDGE_CURVE('',#13820,#13826,#4079,.T.);
#17677=EDGE_CURVE('',#13826,#13825,#4080,.T.);
#17678=EDGE_CURVE('',#13822,#13827,#4081,.T.);
#17679=EDGE_CURVE('',#13827,#13826,#4082,.T.);
#17680=EDGE_CURVE('',#13818,#13828,#4083,.T.);
#17681=EDGE_CURVE('',#13828,#13827,#4084,.T.);
#17682=EDGE_CURVE('',#13824,#13828,#4085,.T.);
#17683=EDGE_CURVE('',#13805,#13809,#4086,.T.);
#17684=EDGE_CURVE('',#13795,#13804,#4087,.T.);
#17685=EDGE_CURVE('',#13785,#13794,#4088,.T.);
#17686=EDGE_CURVE('',#13829,#13829,#10966,.T.);
#17687=EDGE_CURVE('',#13830,#13830,#10967,.T.);
#17688=EDGE_CURVE('',#13831,#13831,#10968,.T.);
#17689=EDGE_CURVE('',#13831,#13830,#4089,.T.);
#17690=EDGE_CURVE('',#13829,#13831,#4090,.T.);
#25196=ORIENTED_EDGE('',*,*,#17602,.F.);
#25197=ORIENTED_EDGE('',*,*,#17603,.F.);
#25198=ORIENTED_EDGE('',*,*,#17604,.F.);
#25199=ORIENTED_EDGE('',*,*,#17605,.T.);
#25200=ORIENTED_EDGE('',*,*,#17606,.T.);
#25201=ORIENTED_EDGE('',*,*,#17603,.T.);
#25202=ORIENTED_EDGE('',*,*,#17607,.T.);
#25203=ORIENTED_EDGE('',*,*,#17608,.F.);
#25204=ORIENTED_EDGE('',*,*,#17609,.F.);
#25205=ORIENTED_EDGE('',*,*,#17610,.F.);
#25206=ORIENTED_EDGE('',*,*,#17611,.T.);
#25207=ORIENTED_EDGE('',*,*,#17612,.T.);
#25208=ORIENTED_EDGE('',*,*,#17609,.T.);
#25209=ORIENTED_EDGE('',*,*,#17613,.T.);
#25210=ORIENTED_EDGE('',*,*,#17602,.T.);
#25211=ORIENTED_EDGE('',*,*,#17614,.T.);
#25212=ORIENTED_EDGE('',*,*,#17610,.T.);
#25213=ORIENTED_EDGE('',*,*,#17615,.T.);
#25214=ORIENTED_EDGE('',*,*,#17616,.F.);
#25215=ORIENTED_EDGE('',*,*,#17617,.F.);
#25216=ORIENTED_EDGE('',*,*,#17618,.F.);
#25217=ORIENTED_EDGE('',*,*,#17619,.T.);
#25218=ORIENTED_EDGE('',*,*,#17620,.T.);
#25219=ORIENTED_EDGE('',*,*,#17617,.T.);
#25220=ORIENTED_EDGE('',*,*,#17621,.T.);
#25221=ORIENTED_EDGE('',*,*,#17622,.F.);
#25222=ORIENTED_EDGE('',*,*,#17623,.F.);
#25223=ORIENTED_EDGE('',*,*,#17624,.F.);
#25224=ORIENTED_EDGE('',*,*,#17625,.T.);
#25225=ORIENTED_EDGE('',*,*,#17626,.T.);
#25226=ORIENTED_EDGE('',*,*,#17623,.T.);
#25227=ORIENTED_EDGE('',*,*,#17627,.T.);
#25228=ORIENTED_EDGE('',*,*,#17608,.T.);
#25229=ORIENTED_EDGE('',*,*,#17628,.T.);
#25230=ORIENTED_EDGE('',*,*,#17624,.T.);
#25231=ORIENTED_EDGE('',*,*,#17629,.T.);
#25232=ORIENTED_EDGE('',*,*,#17630,.F.);
#25233=ORIENTED_EDGE('',*,*,#17631,.F.);
#25234=ORIENTED_EDGE('',*,*,#17632,.F.);
#25235=ORIENTED_EDGE('',*,*,#17633,.T.);
#25236=ORIENTED_EDGE('',*,*,#17634,.T.);
#25237=ORIENTED_EDGE('',*,*,#17631,.T.);
#25238=ORIENTED_EDGE('',*,*,#17635,.T.);
#25239=ORIENTED_EDGE('',*,*,#17636,.F.);
#25240=ORIENTED_EDGE('',*,*,#17637,.F.);
#25241=ORIENTED_EDGE('',*,*,#17638,.F.);
#25242=ORIENTED_EDGE('',*,*,#17639,.T.);
#25243=ORIENTED_EDGE('',*,*,#17640,.T.);
#25244=ORIENTED_EDGE('',*,*,#17637,.T.);
#25245=ORIENTED_EDGE('',*,*,#17641,.T.);
#25246=ORIENTED_EDGE('',*,*,#17622,.T.);
#25247=ORIENTED_EDGE('',*,*,#17642,.T.);
#25248=ORIENTED_EDGE('',*,*,#17638,.T.);
#25249=ORIENTED_EDGE('',*,*,#17643,.T.);
#25250=ORIENTED_EDGE('',*,*,#17636,.T.);
#25251=ORIENTED_EDGE('',*,*,#17644,.T.);
#25252=ORIENTED_EDGE('',*,*,#17632,.T.);
#25253=ORIENTED_EDGE('',*,*,#17645,.T.);
#25254=ORIENTED_EDGE('',*,*,#17630,.T.);
#25255=ORIENTED_EDGE('',*,*,#17646,.T.);
#25256=ORIENTED_EDGE('',*,*,#17618,.T.);
#25257=ORIENTED_EDGE('',*,*,#17647,.T.);
#25258=ORIENTED_EDGE('',*,*,#17616,.T.);
#25259=ORIENTED_EDGE('',*,*,#17648,.T.);
#25260=ORIENTED_EDGE('',*,*,#17604,.T.);
#25261=ORIENTED_EDGE('',*,*,#17649,.T.);
#25262=ORIENTED_EDGE('',*,*,#17607,.F.);
#25263=ORIENTED_EDGE('',*,*,#17615,.F.);
#25264=ORIENTED_EDGE('',*,*,#17612,.F.);
#25265=ORIENTED_EDGE('',*,*,#17650,.T.);
#25266=ORIENTED_EDGE('',*,*,#17613,.F.);
#25267=ORIENTED_EDGE('',*,*,#17629,.F.);
#25268=ORIENTED_EDGE('',*,*,#17626,.F.);
#25269=ORIENTED_EDGE('',*,*,#17651,.T.);
#25270=ORIENTED_EDGE('',*,*,#17627,.F.);
#25271=ORIENTED_EDGE('',*,*,#17643,.F.);
#25272=ORIENTED_EDGE('',*,*,#17640,.F.);
#25273=ORIENTED_EDGE('',*,*,#17652,.T.);
#25274=ORIENTED_EDGE('',*,*,#17614,.F.);
#25275=ORIENTED_EDGE('',*,*,#17648,.F.);
#25276=ORIENTED_EDGE('',*,*,#17646,.F.);
#25277=ORIENTED_EDGE('',*,*,#17644,.F.);
#25278=ORIENTED_EDGE('',*,*,#17642,.F.);
#25279=ORIENTED_EDGE('',*,*,#17628,.F.);
#25280=ORIENTED_EDGE('',*,*,#17653,.F.);
#25281=ORIENTED_EDGE('',*,*,#17654,.F.);
#25282=ORIENTED_EDGE('',*,*,#17655,.F.);
#25283=ORIENTED_EDGE('',*,*,#17656,.F.);
#25284=ORIENTED_EDGE('',*,*,#17657,.F.);
#25285=ORIENTED_EDGE('',*,*,#17658,.F.);
#25286=ORIENTED_EDGE('',*,*,#17656,.T.);
#25287=ORIENTED_EDGE('',*,*,#17659,.T.);
#25288=ORIENTED_EDGE('',*,*,#17660,.T.);
#25289=ORIENTED_EDGE('',*,*,#17661,.F.);
#25290=ORIENTED_EDGE('',*,*,#17655,.T.);
#25291=ORIENTED_EDGE('',*,*,#17662,.T.);
#25292=ORIENTED_EDGE('',*,*,#17663,.T.);
#25293=ORIENTED_EDGE('',*,*,#17659,.F.);
#25294=ORIENTED_EDGE('',*,*,#17653,.T.);
#25295=ORIENTED_EDGE('',*,*,#17664,.T.);
#25296=ORIENTED_EDGE('',*,*,#17665,.T.);
#25297=ORIENTED_EDGE('',*,*,#17666,.T.);
#25298=ORIENTED_EDGE('',*,*,#17667,.T.);
#25299=ORIENTED_EDGE('',*,*,#17664,.F.);
#25300=ORIENTED_EDGE('',*,*,#17658,.T.);
#25301=ORIENTED_EDGE('',*,*,#17668,.T.);
#25302=ORIENTED_EDGE('',*,*,#17654,.T.);
#25303=ORIENTED_EDGE('',*,*,#17666,.F.);
#25304=ORIENTED_EDGE('',*,*,#17669,.T.);
#25305=ORIENTED_EDGE('',*,*,#17662,.F.);
#25306=ORIENTED_EDGE('',*,*,#17670,.T.);
#25307=ORIENTED_EDGE('',*,*,#17668,.F.);
#25308=ORIENTED_EDGE('',*,*,#17657,.T.);
#25309=ORIENTED_EDGE('',*,*,#17661,.T.);
#25310=ORIENTED_EDGE('',*,*,#17663,.F.);
#25311=ORIENTED_EDGE('',*,*,#17671,.T.);
#25312=ORIENTED_EDGE('',*,*,#17672,.T.);
#25313=ORIENTED_EDGE('',*,*,#17673,.F.);
#25314=ORIENTED_EDGE('',*,*,#17669,.F.);
#25315=ORIENTED_EDGE('',*,*,#17674,.T.);
#25316=ORIENTED_EDGE('',*,*,#17675,.T.);
#25317=ORIENTED_EDGE('',*,*,#17671,.F.);
#25318=ORIENTED_EDGE('',*,*,#17665,.F.);
#25319=ORIENTED_EDGE('',*,*,#17676,.T.);
#25320=ORIENTED_EDGE('',*,*,#17677,.T.);
#25321=ORIENTED_EDGE('',*,*,#17674,.F.);
#25322=ORIENTED_EDGE('',*,*,#17667,.F.);
#25323=ORIENTED_EDGE('',*,*,#17678,.T.);
#25324=ORIENTED_EDGE('',*,*,#17679,.T.);
#25325=ORIENTED_EDGE('',*,*,#17676,.F.);
#25326=ORIENTED_EDGE('',*,*,#17670,.F.);
#25327=ORIENTED_EDGE('',*,*,#17680,.T.);
#25328=ORIENTED_EDGE('',*,*,#17681,.T.);
#25329=ORIENTED_EDGE('',*,*,#17678,.F.);
#25330=ORIENTED_EDGE('',*,*,#17660,.F.);
#25331=ORIENTED_EDGE('',*,*,#17673,.T.);
#25332=ORIENTED_EDGE('',*,*,#17682,.T.);
#25333=ORIENTED_EDGE('',*,*,#17680,.F.);
#25334=ORIENTED_EDGE('',*,*,#17675,.F.);
#25335=ORIENTED_EDGE('',*,*,#17677,.F.);
#25336=ORIENTED_EDGE('',*,*,#17679,.F.);
#25337=ORIENTED_EDGE('',*,*,#17681,.F.);
#25338=ORIENTED_EDGE('',*,*,#17682,.F.);
#25339=ORIENTED_EDGE('',*,*,#17672,.F.);
#25340=ORIENTED_EDGE('',*,*,#17605,.F.);
#25341=ORIENTED_EDGE('',*,*,#17650,.F.);
#25342=ORIENTED_EDGE('',*,*,#17611,.F.);
#25343=ORIENTED_EDGE('',*,*,#17651,.F.);
#25344=ORIENTED_EDGE('',*,*,#17625,.F.);
#25345=ORIENTED_EDGE('',*,*,#17652,.F.);
#25346=ORIENTED_EDGE('',*,*,#17639,.F.);
#25347=ORIENTED_EDGE('',*,*,#17683,.F.);
#25348=ORIENTED_EDGE('',*,*,#17633,.F.);
#25349=ORIENTED_EDGE('',*,*,#17684,.F.);
#25350=ORIENTED_EDGE('',*,*,#17619,.F.);
#25351=ORIENTED_EDGE('',*,*,#17685,.F.);
#25352=ORIENTED_EDGE('',*,*,#17686,.T.);
#25353=ORIENTED_EDGE('',*,*,#17634,.F.);
#25354=ORIENTED_EDGE('',*,*,#17683,.T.);
#25355=ORIENTED_EDGE('',*,*,#17641,.F.);
#25356=ORIENTED_EDGE('',*,*,#17645,.F.);
#25357=ORIENTED_EDGE('',*,*,#17620,.F.);
#25358=ORIENTED_EDGE('',*,*,#17684,.T.);
#25359=ORIENTED_EDGE('',*,*,#17635,.F.);
#25360=ORIENTED_EDGE('',*,*,#17647,.F.);
#25361=ORIENTED_EDGE('',*,*,#17606,.F.);
#25362=ORIENTED_EDGE('',*,*,#17685,.T.);
#25363=ORIENTED_EDGE('',*,*,#17621,.F.);
#25364=ORIENTED_EDGE('',*,*,#17649,.F.);
#25365=ORIENTED_EDGE('',*,*,#17687,.F.);
#25366=ORIENTED_EDGE('',*,*,#17688,.F.);
#25367=ORIENTED_EDGE('',*,*,#17689,.T.);
#25368=ORIENTED_EDGE('',*,*,#17687,.T.);
#25369=ORIENTED_EDGE('',*,*,#17689,.F.);
#25370=ORIENTED_EDGE('',*,*,#17686,.F.);
#25371=ORIENTED_EDGE('',*,*,#17690,.T.);
#25372=ORIENTED_EDGE('',*,*,#17688,.T.);
#25373=ORIENTED_EDGE('',*,*,#17690,.F.);
#27138=ADVANCED_FACE('',(#8314),#1708,.T.);
#27139=ADVANCED_FACE('',(#8315),#1709,.T.);
#27140=ADVANCED_FACE('',(#8316),#1710,.T.);
#27141=ADVANCED_FACE('',(#8317),#1711,.T.);
#27142=ADVANCED_FACE('',(#8318),#1712,.T.);
#27143=ADVANCED_FACE('',(#8319),#1713,.T.);
#27144=ADVANCED_FACE('',(#8320),#1714,.T.);
#27145=ADVANCED_FACE('',(#8321),#1715,.T.);
#27146=ADVANCED_FACE('',(#8322),#1716,.T.);
#27147=ADVANCED_FACE('',(#8323),#1717,.T.);
#27148=ADVANCED_FACE('',(#8324),#1718,.T.);
#27149=ADVANCED_FACE('',(#8325),#1719,.T.);
#27150=ADVANCED_FACE('',(#8326),#1720,.T.);
#27151=ADVANCED_FACE('',(#8327),#1721,.T.);
#27152=ADVANCED_FACE('',(#8328),#1722,.T.);
#27153=ADVANCED_FACE('',(#8329),#1723,.T.);
#27154=ADVANCED_FACE('',(#8330),#1724,.T.);
#27155=ADVANCED_FACE('',(#8331),#1725,.T.);
#27156=ADVANCED_FACE('',(#8332),#1726,.T.);
#27157=ADVANCED_FACE('',(#8333),#1727,.T.);
#27158=ADVANCED_FACE('',(#8334),#1728,.T.);
#27159=ADVANCED_FACE('',(#8335,#754),#1729,.T.);
#27160=ADVANCED_FACE('',(#8336),#1730,.T.);
#27161=ADVANCED_FACE('',(#8337),#1731,.T.);
#27162=ADVANCED_FACE('',(#8338),#1732,.T.);
#27163=ADVANCED_FACE('',(#8339),#1733,.T.);
#27164=ADVANCED_FACE('',(#8340),#1734,.T.);
#27165=ADVANCED_FACE('',(#8341),#1735,.T.);
#27166=ADVANCED_FACE('',(#8342),#1736,.F.);
#27167=ADVANCED_FACE('',(#8343),#1737,.F.);
#27168=ADVANCED_FACE('',(#8344),#1738,.F.);
#27169=ADVANCED_FACE('',(#8345),#1739,.F.);
#27170=ADVANCED_FACE('',(#8346),#1740,.F.);
#27171=ADVANCED_FACE('',(#8347),#1741,.F.);
#27172=ADVANCED_FACE('',(#8348),#1742,.F.);
#27173=ADVANCED_FACE('',(#8349,#755),#1743,.F.);
#27174=ADVANCED_FACE('',(#8350),#1744,.T.);
#27175=ADVANCED_FACE('',(#8351),#1745,.T.);
#27176=ADVANCED_FACE('',(#8352),#1746,.T.);
#27177=ADVANCED_FACE('',(#8353),#1747,.T.);
#27178=ADVANCED_FACE('',(#8354),#410,.T.);
#27179=ADVANCED_FACE('',(#8355),#6799,.T.);
#27239=CLOSED_SHELL('',(#27138,#27139,#27140,#27141,#27142,#27143,#27144,
#27145,#27146,#27147,#27148,#27149,#27150,#27151,#27152,#27153,#27154,#27155,
#27156,#27157,#27158,#27159,#27160,#27161,#27162,#27163,#27164,#27165,#27166,
#27167,#27168,#27169,#27170,#27171,#27172,#27173,#27174,#27175,#27176,#27177,
#27178,#27179));
#29846=AXIS2_PLACEMENT_3D('',#53434,#36991,#36992);
#29847=AXIS2_PLACEMENT_3D('',#53435,#36993,#36994);
#29848=AXIS2_PLACEMENT_3D('',#53442,#36998,#36999);
#29849=AXIS2_PLACEMENT_3D('',#53448,#37003,#37004);
#29850=AXIS2_PLACEMENT_3D('',#53455,#37008,#37009);
#29851=AXIS2_PLACEMENT_3D('',#53461,#37013,#37014);
#29852=AXIS2_PLACEMENT_3D('',#53464,#37017,#37018);
#29853=AXIS2_PLACEMENT_3D('',#53471,#37022,#37023);
#29854=AXIS2_PLACEMENT_3D('',#53477,#37027,#37028);
#29855=AXIS2_PLACEMENT_3D('',#53484,#37032,#37033);
#29856=AXIS2_PLACEMENT_3D('',#53490,#37037,#37038);
#29857=AXIS2_PLACEMENT_3D('',#53493,#37041,#37042);
#29858=AXIS2_PLACEMENT_3D('',#53500,#37046,#37047);
#29859=AXIS2_PLACEMENT_3D('',#53506,#37051,#37052);
#29860=AXIS2_PLACEMENT_3D('',#53513,#37056,#37057);
#29861=AXIS2_PLACEMENT_3D('',#53519,#37061,#37062);
#29862=AXIS2_PLACEMENT_3D('',#53522,#37065,#37066);
#29863=AXIS2_PLACEMENT_3D('',#53525,#37069,#37070);
#29864=AXIS2_PLACEMENT_3D('',#53528,#37073,#37074);
#29865=AXIS2_PLACEMENT_3D('',#53531,#37077,#37078);
#29866=AXIS2_PLACEMENT_3D('',#53533,#37080,#37081);
#29867=AXIS2_PLACEMENT_3D('',#53535,#37083,#37084);
#29868=AXIS2_PLACEMENT_3D('',#53537,#37086,#37087);
#29869=AXIS2_PLACEMENT_3D('',#53550,#37094,#37095);
#29870=AXIS2_PLACEMENT_3D('',#53556,#37099,#37100);
#29871=AXIS2_PLACEMENT_3D('',#53560,#37103,#37104);
#29872=AXIS2_PLACEMENT_3D('',#53566,#37108,#37109);
#29873=AXIS2_PLACEMENT_3D('',#53570,#37112,#37113);
#29874=AXIS2_PLACEMENT_3D('',#53572,#37115,#37116);
#29875=AXIS2_PLACEMENT_3D('',#53574,#37118,#37119);
#29876=AXIS2_PLACEMENT_3D('',#53580,#37123,#37124);
#29877=AXIS2_PLACEMENT_3D('',#53584,#37127,#37128);
#29878=AXIS2_PLACEMENT_3D('',#53588,#37131,#37132);
#29879=AXIS2_PLACEMENT_3D('',#53592,#37135,#37136);
#29880=AXIS2_PLACEMENT_3D('',#53596,#37139,#37140);
#29881=AXIS2_PLACEMENT_3D('',#53598,#37142,#37143);
#29882=AXIS2_PLACEMENT_3D('',#53599,#37144,#37145);
#29883=AXIS2_PLACEMENT_3D('',#53604,#37149,#37150);
#29884=AXIS2_PLACEMENT_3D('',#53605,#37151,#37152);
#29885=AXIS2_PLACEMENT_3D('',#53606,#37153,#37154);
#29886=AXIS2_PLACEMENT_3D('',#53607,#37155,#37156);
#29887=AXIS2_PLACEMENT_3D('',#53608,#37157,#37158);
#29888=AXIS2_PLACEMENT_3D('',#53610,#37159,#37160);
#29889=AXIS2_PLACEMENT_3D('',#53611,#37161,#37162);
#29890=AXIS2_PLACEMENT_3D('',#53613,#37163,#37164);
#29891=AXIS2_PLACEMENT_3D('',#53615,#37166,#37167);
#36991=DIRECTION('axis',(0.,0.,1.));
#36992=DIRECTION('refdir',(1.,0.,0.));
#36993=DIRECTION('center_axis',(0.547750005235851,-0.72455327535185,0.418321028566615));
#36994=DIRECTION('ref_axis',(0.606949534647157,0.,-0.794740374205061));
#36995=DIRECTION('',(0.677497944020809,0.0907675134870615,-0.729902592366237));
#36996=DIRECTION('',(0.,0.499999999999999,0.866025403784439));
#36997=DIRECTION('',(-0.677497944020809,-0.677497944020809,-0.286344323664976));
#36998=DIRECTION('center_axis',(0.,-0.866025403784439,0.5));
#36999=DIRECTION('ref_axis',(0.,-0.5,-0.866025403784439));
#37000=DIRECTION('',(0.,-0.5,-0.866025403784439));
#37001=DIRECTION('',(1.,0.,0.));
#37002=DIRECTION('',(-1.,0.,0.));
#37003=DIRECTION('center_axis',(0.547750005235853,0.,0.83664205713323));
#37004=DIRECTION('ref_axis',(0.83664205713323,0.,-0.547750005235853));
#37005=DIRECTION('',(0.67749794402081,-0.586730430533748,-0.44355826870126));
#37006=DIRECTION('',(0.,1.,0.));
#37007=DIRECTION('',(-0.677497944020809,-0.586730430533747,0.443558268701262));
#37008=DIRECTION('center_axis',(0.,0.,1.));
#37009=DIRECTION('ref_axis',(1.,0.,0.));
#37010=DIRECTION('',(0.,-1.,0.));
#37011=DIRECTION('',(1.,0.,0.));
#37012=DIRECTION('',(-1.,0.,0.));
#37013=DIRECTION('center_axis',(0.707106781186548,-0.353553390593274,0.612372435695794));
#37014=DIRECTION('ref_axis',(0.654653670707977,0.,-0.755928946018455));
#37015=DIRECTION('',(0.,0.866025403784439,0.5));
#37016=DIRECTION('',(0.,-0.866025403784439,-0.5));
#37017=DIRECTION('center_axis',(0.547750005235853,-0.72455327535185,-0.418321028566614));
#37018=DIRECTION('ref_axis',(-0.606949534647155,0.,-0.794740374205062));
#37019=DIRECTION('',(0.677497944020809,0.677497944020809,-0.286344323664976));
#37020=DIRECTION('',(0.,-0.499999999999999,0.866025403784439));
#37021=DIRECTION('',(-0.67749794402081,-0.0907675134870647,-0.729902592366236));
#37022=DIRECTION('center_axis',(0.,-0.866025403784439,-0.499999999999999));
#37023=DIRECTION('ref_axis',(0.,0.499999999999999,-0.866025403784439));
#37024=DIRECTION('',(0.,0.499999999999999,-0.866025403784439));
#37025=DIRECTION('',(1.,0.,0.));
#37026=DIRECTION('',(-1.,0.,0.));
#37027=DIRECTION('center_axis',(0.54775000523585,0.72455327535185,0.418321028566616));
#37028=DIRECTION('ref_axis',(0.606949534647158,0.,-0.79474037420506));
#37029=DIRECTION('',(0.67749794402081,-0.67749794402081,0.286344323664975));
#37030=DIRECTION('',(0.,0.5,-0.866025403784439));
#37031=DIRECTION('',(-0.677497944020809,0.0907675134870601,0.729902592366237));
#37032=DIRECTION('center_axis',(0.,0.866025403784439,0.5));
#37033=DIRECTION('ref_axis',(1.,0.,0.));
#37034=DIRECTION('',(0.,-0.5,0.866025403784439));
#37035=DIRECTION('',(1.,0.,0.));
#37036=DIRECTION('',(-1.,0.,0.));
#37037=DIRECTION('center_axis',(0.707106781186547,0.353553390593274,0.612372435695795));
#37038=DIRECTION('ref_axis',(0.654653670707977,0.,-0.755928946018454));
#37039=DIRECTION('',(0.,0.866025403784439,-0.5));
#37040=DIRECTION('',(0.,-0.866025403784439,0.5));
#37041=DIRECTION('center_axis',(0.54775000523585,-1.07255430515093E-15,
-0.836642057133232));
#37042=DIRECTION('ref_axis',(-0.836642057133232,0.,-0.54775000523585));
#37043=DIRECTION('',(0.677497944020808,0.58673043053375,0.443558268701259));
#37044=DIRECTION('',(0.,-1.,1.28197512425571E-15));
#37045=DIRECTION('',(-0.67749794402081,0.586730430533747,-0.44355826870126));
#37046=DIRECTION('center_axis',(0.,-1.28197512425571E-15,-1.));
#37047=DIRECTION('ref_axis',(-1.,0.,0.));
#37048=DIRECTION('',(0.,1.,-1.28197512425571E-15));
#37049=DIRECTION('',(1.,0.,0.));
#37050=DIRECTION('',(-1.,0.,0.));
#37051=DIRECTION('center_axis',(0.54775000523585,0.72455327535185,-0.418321028566616));
#37052=DIRECTION('ref_axis',(-0.606949534647158,0.,-0.794740374205059));
#37053=DIRECTION('',(0.677497944020809,-0.0907675134870586,0.729902592366237));
#37054=DIRECTION('',(0.,-0.500000000000001,-0.866025403784438));
#37055=DIRECTION('',(-0.677497944020809,0.677497944020809,0.286344323664978));
#37056=DIRECTION('center_axis',(0.,0.866025403784438,-0.500000000000001));
#37057=DIRECTION('ref_axis',(-1.,0.,0.));
#37058=DIRECTION('',(0.,0.500000000000001,0.866025403784438));
#37059=DIRECTION('',(1.,0.,0.));
#37060=DIRECTION('',(-1.,0.,0.));
#37061=DIRECTION('center_axis',(0.707106781186548,0.707106781186548,-1.94248565072931E-16));
#37062=DIRECTION('ref_axis',(-2.74708955197652E-16,0.,-1.));
#37063=DIRECTION('',(0.,-2.74708955197652E-16,-1.));
#37064=DIRECTION('',(0.,2.74708955197652E-16,1.));
#37065=DIRECTION('center_axis',(0.707106781186547,0.353553390593274,-0.612372435695795));
#37066=DIRECTION('ref_axis',(-0.654653670707978,0.,-0.755928946018454));
#37067=DIRECTION('',(0.,-0.866025403784439,-0.5));
#37068=DIRECTION('',(0.,0.866025403784439,0.5));
#37069=DIRECTION('center_axis',(0.707106781186548,-0.353553390593274,-0.612372435695794));
#37070=DIRECTION('ref_axis',(-0.654653670707977,0.,-0.755928946018455));
#37071=DIRECTION('',(0.,-0.866025403784439,0.5));
#37072=DIRECTION('',(0.,0.866025403784439,-0.5));
#37073=DIRECTION('center_axis',(0.707106781186548,-0.707106781186548,-9.71242825364656E-17));
#37074=DIRECTION('ref_axis',(-1.37354477598826E-16,0.,-1.));
#37075=DIRECTION('',(0.,-1.37354477598826E-16,1.));
#37076=DIRECTION('',(0.,1.37354477598826E-16,-1.));
#37077=DIRECTION('center_axis',(0.,-0.5,0.866025403784439));
#37078=DIRECTION('ref_axis',(0.,-0.866025403784439,-0.5));
#37079=DIRECTION('',(0.,-0.866025403784439,-0.5));
#37080=DIRECTION('center_axis',(0.,0.5,0.866025403784439));
#37081=DIRECTION('ref_axis',(0.,-0.866025403784439,0.5));
#37082=DIRECTION('',(0.,-0.866025403784439,0.5));
#37083=DIRECTION('center_axis',(0.,1.,-2.74708955197652E-16));
#37084=DIRECTION('ref_axis',(0.,2.74708955197652E-16,1.));
#37085=DIRECTION('',(0.,2.74708955197652E-16,1.));
#37086=DIRECTION('center_axis',(1.,0.,0.));
#37087=DIRECTION('ref_axis',(0.,0.,-1.));
#37088=DIRECTION('',(0.,-0.866025403784439,0.5));
#37089=DIRECTION('',(0.,3.20493781063927E-16,1.));
#37090=DIRECTION('',(0.,0.866025403784439,0.5));
#37091=DIRECTION('',(0.,0.866025403784439,-0.5));
#37092=DIRECTION('',(0.,1.60246890531964E-16,-1.));
#37093=DIRECTION('',(0.,-0.866025403784439,-0.5));
#37094=DIRECTION('center_axis',(0.707106781186547,0.353553390593274,0.612372435695795));
#37095=DIRECTION('ref_axis',(0.654653670707978,0.,-0.755928946018454));
#37096=DIRECTION('',(-0.654653670707977,-4.69765578524213E-16,0.755928946018454));
#37097=DIRECTION('',(0.,-0.866025403784439,0.5));
#37098=DIRECTION('',(-0.654653670707978,0.654653670707977,0.377964473009227));
#37099=DIRECTION('center_axis',(0.707106781186548,-0.353553390593273,0.612372435695795));
#37100=DIRECTION('ref_axis',(0.654653670707977,0.,-0.755928946018455));
#37101=DIRECTION('',(-0.654653670707977,-0.654653670707976,0.377964473009229));
#37102=DIRECTION('',(0.,-0.866025403784439,-0.5));
#37103=DIRECTION('center_axis',(0.707106781186547,-0.353553390593274,-0.612372435695795));
#37104=DIRECTION('ref_axis',(-0.654653670707978,0.,-0.755928946018454));
#37105=DIRECTION('',(-0.654653670707977,1.00453536761267E-15,-0.755928946018454));
#37106=DIRECTION('',(0.,0.866025403784439,-0.5));
#37107=DIRECTION('',(0.654653670707978,0.654653670707977,0.377964473009227));
#37108=DIRECTION('center_axis',(0.707106781186548,0.353553390593274,-0.612372435695794));
#37109=DIRECTION('ref_axis',(-0.654653670707977,0.,-0.755928946018455));
#37110=DIRECTION('',(0.,0.866025403784439,0.5));
#37111=DIRECTION('',(-0.654653670707977,0.654653670707977,-0.377964473009228));
#37112=DIRECTION('center_axis',(0.707106781186547,-0.707106781186548,2.2662332591842E-16));
#37113=DIRECTION('ref_axis',(3.20493781063928E-16,0.,-1.));
#37114=DIRECTION('',(0.,-3.20493781063927E-16,-1.));
#37115=DIRECTION('center_axis',(0.707106781186547,0.707106781186548,1.1331166295921E-16));
#37116=DIRECTION('ref_axis',(1.60246890531964E-16,0.,-1.));
#37117=DIRECTION('',(0.,-1.60246890531964E-16,1.));
#37118=DIRECTION('center_axis',(0.,0.5,-0.866025403784439));
#37119=DIRECTION('ref_axis',(0.,-0.866025403784439,-0.5));
#37120=DIRECTION('',(-1.,0.,0.));
#37121=DIRECTION('',(0.,-0.866025403784439,-0.5));
#37122=DIRECTION('',(-1.,0.,0.));
#37123=DIRECTION('center_axis',(0.,1.,-3.20493781063927E-16));
#37124=DIRECTION('ref_axis',(0.,-3.20493781063927E-16,-1.));
#37125=DIRECTION('',(-1.,0.,0.));
#37126=DIRECTION('',(0.,-3.20493781063927E-16,-1.));
#37127=DIRECTION('center_axis',(0.,0.5,0.866025403784439));
#37128=DIRECTION('ref_axis',(0.,0.866025403784439,-0.5));
#37129=DIRECTION('',(-1.,0.,0.));
#37130=DIRECTION('',(0.,0.866025403784439,-0.5));
#37131=DIRECTION('center_axis',(0.,-0.5,0.866025403784439));
#37132=DIRECTION('ref_axis',(0.,0.866025403784439,0.5));
#37133=DIRECTION('',(-1.,0.,0.));
#37134=DIRECTION('',(0.,0.866025403784439,0.5));
#37135=DIRECTION('center_axis',(0.,-1.,-1.60246890531964E-16));
#37136=DIRECTION('ref_axis',(0.,-1.60246890531964E-16,1.));
#37137=DIRECTION('',(-1.,0.,0.));
#37138=DIRECTION('',(0.,-1.60246890531964E-16,1.));
#37139=DIRECTION('center_axis',(0.,-0.5,-0.866025403784439));
#37140=DIRECTION('ref_axis',(0.,-0.866025403784439,0.5));
#37141=DIRECTION('',(0.,-0.866025403784439,0.5));
#37142=DIRECTION('center_axis',(-1.,0.,0.));
#37143=DIRECTION('ref_axis',(0.,0.,1.));
#37144=DIRECTION('center_axis',(1.,0.,0.));
#37145=DIRECTION('ref_axis',(0.,0.,-1.));
#37146=DIRECTION('',(0.,0.866025403784439,0.5));
#37147=DIRECTION('',(0.,0.866025403784439,-0.5));
#37148=DIRECTION('',(0.,1.37354477598826E-16,-1.));
#37149=DIRECTION('center_axis',(1.,0.,0.));
#37150=DIRECTION('ref_axis',(0.,0.,-1.));
#37151=DIRECTION('center_axis',(0.,0.5,-0.866025403784439));
#37152=DIRECTION('ref_axis',(0.,0.866025403784439,0.5));
#37153=DIRECTION('center_axis',(0.,-0.5,-0.866025403784439));
#37154=DIRECTION('ref_axis',(0.,0.866025403784439,-0.5));
#37155=DIRECTION('center_axis',(0.,-1.,-1.37354477598826E-16));
#37156=DIRECTION('ref_axis',(0.,1.37354477598826E-16,-1.));
#37157=DIRECTION('center_axis',(-1.,0.,0.));
#37158=DIRECTION('ref_axis',(0.,0.,1.));
#37159=DIRECTION('center_axis',(1.,0.,0.));
#37160=DIRECTION('ref_axis',(0.,0.,-1.));
#37161=DIRECTION('center_axis',(1.,0.,0.));
#37162=DIRECTION('ref_axis',(0.,1.,0.));
#37163=DIRECTION('center_axis',(1.,0.,0.));
#37164=DIRECTION('ref_axis',(0.,0.,-1.));
#37165=DIRECTION('',(-0.707106781186548,0.707106781186547,8.65956056235492E-17));
#37166=DIRECTION('center_axis',(1.,0.,0.));
#37167=DIRECTION('ref_axis',(0.,1.,0.));
#37168=DIRECTION('',(-1.,0.,0.));
#53434=CARTESIAN_POINT('',(0.,0.,0.));
#53435=CARTESIAN_POINT('Origin',(5.5,-7.,3.54145188432738));
#53436=CARTESIAN_POINT('',(5.5,-6.56698729810778,4.29145188432738));
#53437=CARTESIAN_POINT('',(6.,-6.5,3.75277674973257));
#53438=CARTESIAN_POINT('',(5.5,-6.56698729810778,4.29145188432738));
#53439=CARTESIAN_POINT('',(5.5,-7.,3.54145188432738));
#53440=CARTESIAN_POINT('',(5.5,-7.,3.54145188432738));
#53441=CARTESIAN_POINT('',(6.,-6.5,3.75277674973257));
#53442=CARTESIAN_POINT('Origin',(0.,-6.78349364905389,3.91645188432738));
#53443=CARTESIAN_POINT('',(0.,-6.56698729810778,4.29145188432738));
#53444=CARTESIAN_POINT('',(0.,-7.,3.54145188432738));
#53445=CARTESIAN_POINT('',(0.,-6.78349364905389,3.91645188432738));
#53446=CARTESIAN_POINT('',(0.,-7.,3.54145188432738));
#53447=CARTESIAN_POINT('',(0.,-6.56698729810778,4.29145188432738));
#53448=CARTESIAN_POINT('Origin',(5.5,-0.433012701892218,7.83290376865476));
#53449=CARTESIAN_POINT('',(5.5,0.43301270189222,7.83290376865476));
#53450=CARTESIAN_POINT('',(6.,5.55111512312578E-16,7.50555349946513));
#53451=CARTESIAN_POINT('',(5.5,0.43301270189222,7.83290376865476));
#53452=CARTESIAN_POINT('',(5.5,-0.433012701892219,7.83290376865476));
#53453=CARTESIAN_POINT('',(5.5,-0.433012701892218,7.83290376865476));
#53454=CARTESIAN_POINT('',(6.,0.,7.50555349946513));
#53455=CARTESIAN_POINT('Origin',(0.,9.0205620750794E-16,7.83290376865476));
#53456=CARTESIAN_POINT('',(0.,0.43301270189222,7.83290376865476));
#53457=CARTESIAN_POINT('',(0.,-0.433012701892219,7.83290376865476));
#53458=CARTESIAN_POINT('',(0.,4.5102810375397E-16,7.83290376865476));
#53459=CARTESIAN_POINT('',(0.,-0.433012701892218,7.83290376865476));
#53460=CARTESIAN_POINT('',(0.,0.43301270189222,7.83290376865476));
#53461=CARTESIAN_POINT('Origin',(5.75,-1.625,6.85603444662681));
#53462=CARTESIAN_POINT('',(6.,-1.5,6.6395280956807));
#53463=CARTESIAN_POINT('',(5.5,-1.75,7.07254079757292));
#53464=CARTESIAN_POINT('Origin',(5.5,-6.56698729810778,-4.29145188432738));
#53465=CARTESIAN_POINT('',(5.5,-7.,-3.54145188432738));
#53466=CARTESIAN_POINT('',(6.,-6.5,-3.75277674973257));
#53467=CARTESIAN_POINT('',(5.5,-7.,-3.54145188432738));
#53468=CARTESIAN_POINT('',(5.5,-6.56698729810778,-4.29145188432738));
#53469=CARTESIAN_POINT('',(5.5,-6.56698729810778,-4.29145188432738));
#53470=CARTESIAN_POINT('',(6.,-6.5,-3.75277674973257));
#53471=CARTESIAN_POINT('Origin',(0.,-6.78349364905389,-3.91645188432738));
#53472=CARTESIAN_POINT('',(0.,-7.,-3.54145188432738));
#53473=CARTESIAN_POINT('',(0.,-6.56698729810778,-4.29145188432738));
#53474=CARTESIAN_POINT('',(0.,-6.78349364905389,-3.91645188432738));
#53475=CARTESIAN_POINT('',(0.,-6.56698729810778,-4.29145188432738));
#53476=CARTESIAN_POINT('',(0.,-7.,-3.54145188432738));
#53477=CARTESIAN_POINT('Origin',(5.5,6.56698729810778,4.29145188432738));
#53478=CARTESIAN_POINT('',(5.5,7.,3.54145188432738));
#53479=CARTESIAN_POINT('',(6.,6.5,3.75277674973257));
#53480=CARTESIAN_POINT('',(5.5,7.,3.54145188432738));
#53481=CARTESIAN_POINT('',(5.5,6.56698729810778,4.29145188432738));
#53482=CARTESIAN_POINT('',(5.5,6.56698729810778,4.29145188432738));
#53483=CARTESIAN_POINT('',(6.,6.5,3.75277674973257));
#53484=CARTESIAN_POINT('Origin',(0.,6.78349364905389,3.91645188432738));
#53485=CARTESIAN_POINT('',(0.,7.,3.54145188432738));
#53486=CARTESIAN_POINT('',(0.,6.56698729810778,4.29145188432738));
#53487=CARTESIAN_POINT('',(0.,6.78349364905389,3.91645188432738));
#53488=CARTESIAN_POINT('',(0.,6.56698729810778,4.29145188432738));
#53489=CARTESIAN_POINT('',(0.,7.,3.54145188432738));
#53490=CARTESIAN_POINT('Origin',(5.75,5.125,4.83530850446312));
#53491=CARTESIAN_POINT('',(6.,5.,4.61880215351701));
#53492=CARTESIAN_POINT('',(5.5,5.25,5.05181485540922));
#53493=CARTESIAN_POINT('Origin',(5.5,0.433012701892218,-7.83290376865476));
#53494=CARTESIAN_POINT('',(5.5,-0.433012701892222,-7.83290376865476));
#53495=CARTESIAN_POINT('',(6.,0.,-7.50555349946514));
#53496=CARTESIAN_POINT('',(5.5,-0.433012701892221,-7.83290376865476));
#53497=CARTESIAN_POINT('',(5.5,0.433012701892217,-7.83290376865476));
#53498=CARTESIAN_POINT('',(5.5,0.433012701892218,-7.83290376865476));
#53499=CARTESIAN_POINT('',(6.,-1.11022302462516E-15,-7.50555349946514));
#53500=CARTESIAN_POINT('Origin',(0.,-2.22044604925031E-15,-7.83290376865476));
#53501=CARTESIAN_POINT('',(0.,-0.433012701892223,-7.83290376865476));
#53502=CARTESIAN_POINT('',(0.,0.433012701892217,-7.83290376865476));
#53503=CARTESIAN_POINT('',(0.,-6.13101691567725E-15,-7.83290376865476));
#53504=CARTESIAN_POINT('',(0.,0.433012701892218,-7.83290376865476));
#53505=CARTESIAN_POINT('',(0.,-0.433012701892222,-7.83290376865476));
#53506=CARTESIAN_POINT('Origin',(5.5,7.,-3.54145188432738));
#53507=CARTESIAN_POINT('',(5.5,6.56698729810778,-4.29145188432738));
#53508=CARTESIAN_POINT('',(6.,6.5,-3.75277674973257));
#53509=CARTESIAN_POINT('',(5.5,6.56698729810778,-4.29145188432739));
#53510=CARTESIAN_POINT('',(5.5,7.,-3.54145188432738));
#53511=CARTESIAN_POINT('',(5.5,7.,-3.54145188432738));
#53512=CARTESIAN_POINT('',(6.,6.5,-3.75277674973257));
#53513=CARTESIAN_POINT('Origin',(0.,6.78349364905389,-3.91645188432738));
#53514=CARTESIAN_POINT('',(0.,6.56698729810778,-4.29145188432739));
#53515=CARTESIAN_POINT('',(0.,7.,-3.54145188432738));
#53516=CARTESIAN_POINT('',(0.,6.78349364905389,-3.91645188432738));
#53517=CARTESIAN_POINT('',(0.,7.,-3.54145188432738));
#53518=CARTESIAN_POINT('',(0.,6.56698729810778,-4.29145188432738));
#53519=CARTESIAN_POINT('Origin',(5.75,6.75,-2.02072594216369));
#53520=CARTESIAN_POINT('',(6.,6.5,-2.02072594216369));
#53521=CARTESIAN_POINT('',(5.5,7.,-2.02072594216369));
#53522=CARTESIAN_POINT('Origin',(5.75,1.625,-6.85603444662681));
#53523=CARTESIAN_POINT('',(6.,1.5,-6.6395280956807));
#53524=CARTESIAN_POINT('',(5.5,1.75,-7.07254079757292));
#53525=CARTESIAN_POINT('Origin',(5.75,-5.125,-4.83530850446312));
#53526=CARTESIAN_POINT('',(6.,-5.,-4.61880215351701));
#53527=CARTESIAN_POINT('',(5.5,-5.25,-5.05181485540923));
#53528=CARTESIAN_POINT('Origin',(5.75,-6.75,2.02072594216369));
#53529=CARTESIAN_POINT('',(6.,-6.5,2.02072594216369));
#53530=CARTESIAN_POINT('',(5.5,-7.,2.02072594216369));
#53531=CARTESIAN_POINT('Origin',(0.,4.94935111404957E-16,8.08290376865476));
#53532=CARTESIAN_POINT('',(0.,4.94935111404957E-16,8.08290376865476));
#53533=CARTESIAN_POINT('Origin',(0.,7.,4.04145188432738));
#53534=CARTESIAN_POINT('',(0.,7.,4.04145188432738));
#53535=CARTESIAN_POINT('Origin',(0.,7.,-4.04145188432738));
#53536=CARTESIAN_POINT('',(0.,7.,-4.04145188432738));
#53537=CARTESIAN_POINT('Origin',(6.,0.,0.));
#53538=CARTESIAN_POINT('',(6.,3.5,2.02072594216369));
#53539=CARTESIAN_POINT('',(6.,-5.55111512312578E-16,4.04145188432738));
#53540=CARTESIAN_POINT('',(6.,1.,3.46410161513775));
#53541=CARTESIAN_POINT('',(6.,3.5,-2.02072594216369));
#53542=CARTESIAN_POINT('',(6.,3.5,0.866025403784438));
#53543=CARTESIAN_POINT('',(6.,-5.55111512312578E-16,-4.04145188432738));
#53544=CARTESIAN_POINT('',(6.,2.5,-2.59807621135332));
#53545=CARTESIAN_POINT('',(6.,-3.5,-2.02072594216369));
#53546=CARTESIAN_POINT('',(6.,-1.,-3.46410161513775));
#53547=CARTESIAN_POINT('',(6.,-3.5,2.02072594216369));
#53548=CARTESIAN_POINT('',(6.,-3.5,-0.866025403784439));
#53549=CARTESIAN_POINT('',(6.,-2.5,2.59807621135332));
#53550=CARTESIAN_POINT('Origin',(5.75,-0.875,-3.24759526419165));
#53551=CARTESIAN_POINT('',(5.5,-6.36345143234944E-16,-3.46410161513775));
#53552=CARTESIAN_POINT('',(6.,-2.77555756156289E-16,-4.04145188432738));
#53553=CARTESIAN_POINT('',(5.5,-3.,-1.73205080756888));
#53554=CARTESIAN_POINT('',(5.5,-0.75,-3.03108891324554));
#53555=CARTESIAN_POINT('',(6.,-3.5,-2.02072594216369));
#53556=CARTESIAN_POINT('Origin',(5.75,2.375,-2.38156986040721));
#53557=CARTESIAN_POINT('',(5.5,3.,-1.73205080756888));
#53558=CARTESIAN_POINT('',(6.,3.5,-2.02072594216369));
#53559=CARTESIAN_POINT('',(5.5,2.25,-2.1650635094611));
#53560=CARTESIAN_POINT('Origin',(5.75,0.875,3.24759526419165));
#53561=CARTESIAN_POINT('',(5.5,2.12115047744981E-16,3.46410161513775));
#53562=CARTESIAN_POINT('',(6.,-5.55111512312578E-16,4.04145188432738));
#53563=CARTESIAN_POINT('',(5.5,3.,1.73205080756888));
#53564=CARTESIAN_POINT('',(5.5,0.75,3.03108891324554));
#53565=CARTESIAN_POINT('',(5.5,3.,1.73205080756888));
#53566=CARTESIAN_POINT('Origin',(5.75,-2.375,2.38156986040721));
#53567=CARTESIAN_POINT('',(5.5,-3.,1.73205080756888));
#53568=CARTESIAN_POINT('',(5.5,-2.25,2.1650635094611));
#53569=CARTESIAN_POINT('',(6.,-3.5,2.02072594216369));
#53570=CARTESIAN_POINT('Origin',(5.75,3.25,0.866025403784438));
#53571=CARTESIAN_POINT('',(5.5,3.,0.866025403784438));
#53572=CARTESIAN_POINT('Origin',(5.75,-3.25,-0.866025403784439));
#53573=CARTESIAN_POINT('',(5.5,-3.,-0.866025403784439));
#53574=CARTESIAN_POINT('Origin',(6.,3.,-1.73205080756888));
#53575=CARTESIAN_POINT('',(2.5,3.,-1.73205080756888));
#53576=CARTESIAN_POINT('',(6.,3.,-1.73205080756888));
#53577=CARTESIAN_POINT('',(2.5,-5.55111512312578E-16,-3.46410161513775));
#53578=CARTESIAN_POINT('',(2.5,-6.36345143234944E-16,-3.46410161513775));
#53579=CARTESIAN_POINT('',(6.,-6.36345143234944E-16,-3.46410161513775));
#53580=CARTESIAN_POINT('Origin',(6.,3.,1.73205080756888));
#53581=CARTESIAN_POINT('',(2.5,3.,1.73205080756888));
#53582=CARTESIAN_POINT('',(6.,3.,1.73205080756888));
#53583=CARTESIAN_POINT('',(2.5,3.,-1.73205080756888));
#53584=CARTESIAN_POINT('Origin',(6.,0.,3.46410161513775));
#53585=CARTESIAN_POINT('',(2.5,0.,3.46410161513775));
#53586=CARTESIAN_POINT('',(6.,2.12115047744981E-16,3.46410161513775));
#53587=CARTESIAN_POINT('',(2.5,3.,1.73205080756888));
#53588=CARTESIAN_POINT('Origin',(6.,-3.,1.73205080756888));
#53589=CARTESIAN_POINT('',(2.5,-3.,1.73205080756888));
#53590=CARTESIAN_POINT('',(6.,-3.,1.73205080756888));
#53591=CARTESIAN_POINT('',(2.5,2.12115047744981E-16,3.46410161513775));
#53592=CARTESIAN_POINT('Origin',(6.,-3.,-1.73205080756888));
#53593=CARTESIAN_POINT('',(2.5,-3.,-1.73205080756888));
#53594=CARTESIAN_POINT('',(6.,-3.,-1.73205080756888));
#53595=CARTESIAN_POINT('',(2.5,-3.,1.73205080756888));
#53596=CARTESIAN_POINT('Origin',(6.,-5.55111512312578E-16,-3.46410161513775));
#53597=CARTESIAN_POINT('',(2.5,-3.,-1.73205080756888));
#53598=CARTESIAN_POINT('Origin',(2.5,0.,0.));
#53599=CARTESIAN_POINT('Origin',(0.,0.,0.));
#53600=CARTESIAN_POINT('',(0.,-1.48480533421487E-15,-8.08290376865476));
#53601=CARTESIAN_POINT('',(0.,-7.,-4.04145188432738));
#53602=CARTESIAN_POINT('',(0.,-7.,4.04145188432738));
#53603=CARTESIAN_POINT('',(0.,-6.85,-8.38883057415937E-16));
#53604=CARTESIAN_POINT('Origin',(0.,0.,0.));
#53605=CARTESIAN_POINT('Origin',(0.,-1.48480533421487E-15,-8.08290376865476));
#53606=CARTESIAN_POINT('Origin',(0.,-7.,-4.04145188432738));
#53607=CARTESIAN_POINT('Origin',(0.,-7.,4.04145188432738));
#53608=CARTESIAN_POINT('Origin',(-10.,6.35,0.));
#53609=CARTESIAN_POINT('',(-10.,-6.35,-7.77650717458569E-16));
#53610=CARTESIAN_POINT('Origin',(-10.,0.,0.));
#53611=CARTESIAN_POINT('Origin',(-9.75,0.,0.));
#53612=CARTESIAN_POINT('',(-9.5,-6.85,-8.38883057415937E-16));
#53613=CARTESIAN_POINT('Origin',(-9.5,0.,0.));
#53614=CARTESIAN_POINT('',(-9.75,-6.6,-8.08266887437253E-16));
#53615=CARTESIAN_POINT('Origin',(-4.75,0.,0.));
#53616=CARTESIAN_POINT('',(-4.75,-6.85,-8.38883057415937E-16));
#55713=UNCERTAINTY_MEASURE_WITH_UNIT(LENGTH_MEASURE(0.01),#55738,
'DISTANCE_ACCURACY_VALUE',
'Maximum model space distance between geometric entities at asserted c
onnectivities');
#55715=UNCERTAINTY_MEASURE_WITH_UNIT(LENGTH_MEASURE(0.01),#55738,
'DISTANCE_ACCURACY_VALUE',
'Maximum model space distance between geometric entities at asserted c
onnectivities');
#55735=(
GEOMETRIC_REPRESENTATION_CONTEXT(3)
GLOBAL_UNCERTAINTY_ASSIGNED_CONTEXT((#55713))
GLOBAL_UNIT_ASSIGNED_CONTEXT((#55738,#55740,#55741))
REPRESENTATION_CONTEXT('','3D')
);
#55737=(
GEOMETRIC_REPRESENTATION_CONTEXT(3)
GLOBAL_UNCERTAINTY_ASSIGNED_CONTEXT((#55715))
GLOBAL_UNIT_ASSIGNED_CONTEXT((#55738,#55740,#55741))
REPRESENTATION_CONTEXT('','3D')
);
#55738=(
LENGTH_UNIT()
NAMED_UNIT(*)
SI_UNIT(.MILLI.,.METRE.)
);
#55740=(
NAMED_UNIT(*)
PLANE_ANGLE_UNIT()
SI_UNIT($,.RADIAN.)
);
#55741=(
NAMED_UNIT(*)
SI_UNIT($,.STERADIAN.)
SOLID_ANGLE_UNIT()
);
#55761=SHAPE_DEFINITION_REPRESENTATION(#55782,#55839);
#55782=PRODUCT_DEFINITION_SHAPE('',$,#55861);
#55839=SHAPE_REPRESENTATION('',(#29846),#55735);
#55841=PRODUCT_DEFINITION_CONTEXT('part definition',#55906,'design');
#55861=PRODUCT_DEFINITION('2026-10-26-00-34-34-597',
'17_Gauge_Plug_1-4_NPT',#55882,#55841);
#55882=PRODUCT_DEFINITION_FORMATION('',$,#55927);
#55906=APPLICATION_CONTEXT(
'Core Data for Automotive Mechanical Design Process');
#55907=PRODUCT_CONTEXT('part definition',#55906,'mechanical');
#55927=PRODUCT('2026-10-26-00-34-34-597','17_Gauge_Plug_1-4_NPT',$,(#55907));
#55978=COLOUR_RGB('Sky Blue',0.24,0.69,0.87);
#55979=FILL_AREA_STYLE_COLOUR('',#55978);
#55980=FILL_AREA_STYLE('',(#55979));
#55981=SURFACE_STYLE_FILL_AREA(#55980);
#55982=SURFACE_SIDE_STYLE('',(#55981));
#55983=SURFACE_STYLE_USAGE(.BOTH.,#55982);
#55984=PRESENTATION_STYLE_ASSIGNMENT((#55983));
ENDSEC;
END-ISO-10303-21;
